ISO-10303-21;
HEADER;
/* Generated by software containing ST-Developer
 * from STEP Tools, Inc. (www.steptools.com) 
 */

FILE_DESCRIPTION(
/* description */ (''),
/* implementation_level */ '2;1');

FILE_NAME(
/* name */ 'Knob.step',
/* time_stamp */ '2026-10-23T17:22:31+06:00',
/* author */ (''),
/* organization */ (''),
/* preprocessor_version */ 'ST-DEVELOPER v20.2',
/* originating_system */ 'Autodesk Translation Framework v15.15.0.0',
/* authorisation */ '');

FILE_SCHEMA (('AUTOMOTIVE_DESIGN { 1 0 10303 214 3 1 1 }'));
ENDSEC;

DATA;
#10=MECHANICAL_DESIGN_GEOMETRIC_PRESENTATION_REPRESENTATION('',(#79),#7315);
#59=SHAPE_REPRESENTATION_RELATIONSHIP('SRR','None',#7355,#69);
#69=ADVANCED_BREP_SHAPE_REPRESENTATION('',(#89),#7307);
#79=STYLED_ITEM('',(#7438),#89);
#89=MANIFOLD_SOLID_BREP('Knob',#3216);
#157=B_SPLINE_CURVE_WITH_KNOTS('',3,(#5698,#5699,#5700,#5701,#5702,#5703,
#5704,#5705,#5706,#5707,#5708,#5709,#5710,#5711,#5712,#5713,#5714,#5715,
#5716,#5717,#5718,#5719),.UNSPECIFIED.,.F.,.F.,(4,2,2,2,2,2,2,2,2,2,4),
(-0.134540802780941,-0.124694593380528,-0.114887429972743,-0.100865411229465,
-0.0874132288816555,-0.0739776319181918,-0.0597069979702496,-0.0456321639023999,
-0.0321262367963484,-0.0169842646851755,-7.43769472487735E-6),
 .UNSPECIFIED.);
#158=B_SPLINE_CURVE_WITH_KNOTS('',3,(#5728,#5729,#5730,#5731,#5732,#5733,
#5734,#5735,#5736,#5737,#5738,#5739,#5740,#5741,#5742,#5743,#5744,#5745,
#5746,#5747,#5748,#5749),.UNSPECIFIED.,.F.,.F.,(4,2,2,2,2,2,2,2,2,2,4),
(-0.134546412264088,-0.12503895955274,-0.115553020431079,-0.101555833168035,
-0.0880617151829101,-0.0742479340082139,-0.0594501685168066,-0.0457182707143297,
-0.0321286187319872,-0.0169925187729982,-7.43769474437564E-6),
 .UNSPECIFIED.);
#159=B_SPLINE_CURVE_WITH_KNOTS('',3,(#5758,#5759,#5760,#5761,#5762,#5763,
#5764,#5765,#5766,#5767,#5768,#5769,#5770,#5771,#5772,#5773,#5774,#5775,
#5776,#5777,#5778,#5779),.UNSPECIFIED.,.F.,.F.,(4,2,2,2,2,2,2,2,2,2,4),
(-0.134546412264079,-0.125038959552735,-0.115553020431074,-0.101555833168028,
-0.0880617151829049,-0.074247934008211,-0.0594501685168069,-0.0457182707143326,
-0.0321286187319901,-0.0169925187729991,-7.43769474460115E-6),
 .UNSPECIFIED.);
#160=B_SPLINE_CURVE_WITH_KNOTS('',3,(#5788,#5789,#5790,#5791,#5792,#5793,
#5794,#5795,#5796,#5797,#5798,#5799,#5800,#5801,#5802,#5803,#5804,#5805,
#5806,#5807,#5808,#5809),.UNSPECIFIED.,.F.,.F.,(4,2,2,2,2,2,2,2,2,2,4),
(-0.134540616537392,-0.124646722470156,-0.114789241819855,-0.100787758586552,
-0.0873465389988059,-0.0739206374616,-0.0596515865040428,-0.0456502398664556,
-0.0321268160753299,-0.0169860369506264,-7.43769472906497E-6),
 .UNSPECIFIED.);
#161=B_SPLINE_CURVE_WITH_KNOTS('',3,(#5818,#5819,#5820,#5821,#5822,#5823,
#5824,#5825,#5826,#5827,#5828,#5829,#5830,#5831,#5832,#5833,#5834,#5835,
#5836,#5837,#5838,#5839,#5840,#5841,#5842,#5843),.UNSPECIFIED.,.F.,.F.,
(4,2,2,2,2,2,2,2,2,2,2,2,4),(-0.134481588819224,-0.12541821251768,-0.116248820382152,
-0.10297112990022,-0.0890270299810203,-0.0783509942952859,-0.0707062224441527,
-0.0638270554385495,-0.0561931432260482,-0.0455507450931791,-0.031889734739909,
-0.0168775831944051,-7.43769447408144E-6),.UNSPECIFIED.);
#162=B_SPLINE_CURVE_WITH_KNOTS('',3,(#5852,#5853,#5854,#5855,#5856,#5857,
#5858,#5859,#5860,#5861,#5862,#5863,#5864,#5865,#5866,#5867,#5868,#5869,
#5870,#5871,#5872,#5873),.UNSPECIFIED.,.F.,.F.,(4,2,2,2,2,2,2,2,2,2,4),
(-0.134540616537393,-0.124646722470158,-0.114789241819856,-0.100787758586554,
-0.087346538998809,-0.0739206374616026,-0.0596515865040475,-0.0456502398664592,
-0.0321268160753317,-0.0169860369506279,-7.43769472906497E-6),
 .UNSPECIFIED.);
#163=B_SPLINE_CURVE_WITH_KNOTS('',3,(#5882,#5883,#5884,#5885,#5886,#5887,
#5888,#5889,#5890,#5891,#5892,#5893,#5894,#5895,#5896,#5897,#5898,#5899,
#5900,#5901,#5902,#5903),.UNSPECIFIED.,.F.,.F.,(4,2,2,2,2,2,2,2,2,2,4),
(-0.134546412264079,-0.125038959552731,-0.115553020431069,-0.101555833168023,
-0.0880617151828988,-0.0742479340082045,-0.0594501685167969,-0.0457182707143222,
-0.0321286187319822,-0.0169925187729959,-7.43769474437564E-6),
 .UNSPECIFIED.);
#164=B_SPLINE_CURVE_WITH_KNOTS('',3,(#5912,#5913,#5914,#5915,#5916,#5917,
#5918,#5919,#5920,#5921,#5922,#5923,#5924,#5925,#5926,#5927,#5928,#5929,
#5930,#5931,#5932,#5933),.UNSPECIFIED.,.F.,.F.,(4,2,2,2,2,2,2,2,2,2,4),
(-0.134546412264076,-0.125038959552731,-0.11555302043107,-0.101555833168024,
-0.0880617151829001,-0.0742479340082053,-0.0594501685167959,-0.0457182707143225,
-0.0321286187319831,-0.0169925187729947,-7.43769474415359E-6),
 .UNSPECIFIED.);
#165=B_SPLINE_CURVE_WITH_KNOTS('',3,(#5942,#5943,#5944,#5945,#5946,#5947,
#5948,#5949,#5950,#5951,#5952,#5953,#5954,#5955,#5956,#5957,#5958,#5959,
#5960,#5961,#5962,#5963),.UNSPECIFIED.,.F.,.F.,(4,2,2,2,2,2,2,2,2,2,4),
(-0.134540802780906,-0.124694593380492,-0.114887429972709,-0.100865411229438,
-0.0874132288816369,-0.0739776319181792,-0.0597069979702393,-0.0456321639023924,
-0.0321262367963445,-0.0169842646851756,-7.43769472488082E-6),
 .UNSPECIFIED.);
#166=B_SPLINE_CURVE_WITH_KNOTS('',3,(#6008,#6009,#6010,#6011,#6012,#6013,
#6014,#6015,#6016,#6017,#6018,#6019),.UNSPECIFIED.,.F.,.F.,(4,2,2,2,2,4),
(-0.0672537780264869,-0.0571863690452376,-0.0459002523768814,-0.0321135744364736,
-0.0170527660266752,0.),.UNSPECIFIED.);
#167=B_SPLINE_CURVE_WITH_KNOTS('',3,(#6022,#6023,#6024,#6025,#6026,#6027,
#6028,#6029,#6030,#6031,#6032,#6033,#6034,#6035,#6036,#6037),
 .UNSPECIFIED.,.F.,.F.,(4,2,2,2,2,2,2,4),(-0.134507884019342,-0.12584488585901,
-0.117135322530839,-0.103482612739793,-0.0895114384281185,-0.0780993566612536,
-0.0676309733624946,-0.0672537780264869),.UNSPECIFIED.);
#291=LINE('',#5696,#451);
#292=LINE('',#5721,#452);
#293=LINE('',#5726,#453);
#294=LINE('',#5751,#454);
#295=LINE('',#5756,#455);
#296=LINE('',#5781,#456);
#297=LINE('',#5786,#457);
#298=LINE('',#5811,#458);
#299=LINE('',#5816,#459);
#300=LINE('',#5845,#460);
#301=LINE('',#5850,#461);
#302=LINE('',#5875,#462);
#303=LINE('',#5880,#463);
#304=LINE('',#5905,#464);
#305=LINE('',#5910,#465);
#306=LINE('',#5935,#466);
#307=LINE('',#5940,#467);
#308=LINE('',#5965,#468);
#309=LINE('',#5986,#469);
#310=LINE('',#6039,#470);
#311=LINE('',#6045,#471);
#451=VECTOR('',#4054,10.);
#452=VECTOR('',#4055,10.);
#453=VECTOR('',#4060,10.);
#454=VECTOR('',#4061,10.);
#455=VECTOR('',#4066,10.);
#456=VECTOR('',#4067,10.);
#457=VECTOR('',#4072,10.);
#458=VECTOR('',#4073,10.);
#459=VECTOR('',#4078,10.);
#460=VECTOR('',#4079,10.);
#461=VECTOR('',#4084,10.);
#462=VECTOR('',#4085,10.);
#463=VECTOR('',#4090,10.);
#464=VECTOR('',#4091,10.);
#465=VECTOR('',#4096,10.);
#466=VECTOR('',#4097,10.);
#467=VECTOR('',#4102,10.);
#468=VECTOR('',#4103,10.);
#469=VECTOR('',#4136,10.);
#470=VECTOR('',#4179,10.);
#471=VECTOR('',#4188,1.);
#603=CYLINDRICAL_SURFACE('',#3468,0.5);
#604=CYLINDRICAL_SURFACE('',#3470,0.5);
#605=CYLINDRICAL_SURFACE('',#3472,0.500000000000001);
#606=CYLINDRICAL_SURFACE('',#3474,0.5);
#607=CYLINDRICAL_SURFACE('',#3476,0.5);
#608=CYLINDRICAL_SURFACE('',#3478,0.5);
#609=CYLINDRICAL_SURFACE('',#3480,0.5);
#610=CYLINDRICAL_SURFACE('',#3482,0.5);
#611=CYLINDRICAL_SURFACE('',#3484,0.5);
#612=CYLINDRICAL_SURFACE('',#3499,2.);
#613=CYLINDRICAL_SURFACE('',#3501,2.);
#614=CYLINDRICAL_SURFACE('',#3503,2.);
#615=CYLINDRICAL_SURFACE('',#3505,2.);
#616=CYLINDRICAL_SURFACE('',#3507,2.);
#617=CYLINDRICAL_SURFACE('',#3509,2.);
#618=CYLINDRICAL_SURFACE('',#3511,2.);
#619=CYLINDRICAL_SURFACE('',#3513,2.);
#620=CYLINDRICAL_SURFACE('',#3515,2.);
#621=CYLINDRICAL_SURFACE('',#3521,0.5);
#622=CYLINDRICAL_SURFACE('',#3522,2.);
#623=CYLINDRICAL_SURFACE('',#3524,1.);
#690=FACE_BOUND('',#987,.T.);
#707=PLANE('',#3486);
#708=PLANE('',#3523);
#709=PLANE('',#3526);
#794=FACE_OUTER_BOUND('',#977,.T.);
#795=FACE_OUTER_BOUND('',#978,.T.);
#796=FACE_OUTER_BOUND('',#979,.T.);
#797=FACE_OUTER_BOUND('',#980,.T.);
#798=FACE_OUTER_BOUND('',#981,.T.);
#799=FACE_OUTER_BOUND('',#982,.T.);
#800=FACE_OUTER_BOUND('',#983,.T.);
#801=FACE_OUTER_BOUND('',#984,.T.);
#802=FACE_OUTER_BOUND('',#985,.T.);
#803=FACE_OUTER_BOUND('',#986,.T.);
#804=FACE_OUTER_BOUND('',#988,.T.);
#805=FACE_OUTER_BOUND('',#989,.T.);
#806=FACE_OUTER_BOUND('',#990,.T.);
#807=FACE_OUTER_BOUND('',#991,.T.);
#808=FACE_OUTER_BOUND('',#992,.T.);
#809=FACE_OUTER_BOUND('',#993,.T.);
#810=FACE_OUTER_BOUND('',#994,.T.);
#811=FACE_OUTER_BOUND('',#995,.T.);
#812=FACE_OUTER_BOUND('',#996,.T.);
#813=FACE_OUTER_BOUND('',#997,.T.);
#814=FACE_OUTER_BOUND('',#998,.T.);
#815=FACE_OUTER_BOUND('',#999,.T.);
#816=FACE_OUTER_BOUND('',#1000,.T.);
#817=FACE_OUTER_BOUND('',#1001,.T.);
#818=FACE_OUTER_BOUND('',#1002,.T.);
#977=EDGE_LOOP('',(#2442,#2443,#2444,#2445));
#978=EDGE_LOOP('',(#2446,#2447,#2448,#2449));
#979=EDGE_LOOP('',(#2450,#2451,#2452,#2453));
#980=EDGE_LOOP('',(#2454,#2455,#2456,#2457));
#981=EDGE_LOOP('',(#2458,#2459,#2460,#2461));
#982=EDGE_LOOP('',(#2462,#2463,#2464,#2465));
#983=EDGE_LOOP('',(#2466,#2467,#2468,#2469));
#984=EDGE_LOOP('',(#2470,#2471,#2472,#2473));
#985=EDGE_LOOP('',(#2474,#2475,#2476,#2477));
#986=EDGE_LOOP('',(#2478,#2479,#2480,#2481,#2482,#2483,#2484,#2485,#2486,
#2487,#2488,#2489,#2490,#2491,#2492,#2493,#2494,#2495,#2496,#2497));
#987=EDGE_LOOP('',(#2498));
#988=EDGE_LOOP('',(#2499,#2500,#2501,#2502));
#989=EDGE_LOOP('',(#2503,#2504,#2505,#2506));
#990=EDGE_LOOP('',(#2507,#2508,#2509,#2510));
#991=EDGE_LOOP('',(#2511,#2512,#2513,#2514));
#992=EDGE_LOOP('',(#2515,#2516,#2517,#2518));
#993=EDGE_LOOP('',(#2519,#2520,#2521,#2522));
#994=EDGE_LOOP('',(#2523,#2524,#2525,#2526));
#995=EDGE_LOOP('',(#2527,#2528,#2529,#2530));
#996=EDGE_LOOP('',(#2531,#2532,#2533,#2534));
#997=EDGE_LOOP('',(#2535,#2536,#2537,#2538,#2539,#2540,#2541,#2542,#2543,
#2544,#2545,#2546,#2547,#2548,#2549,#2550,#2551,#2552,#2553,#2554,#2555,
#2556,#2557,#2558));
#998=EDGE_LOOP('',(#2559,#2560,#2561,#2562,#2563));
#999=EDGE_LOOP('',(#2564,#2565,#2566,#2567));
#1000=EDGE_LOOP('',(#2568));
#1001=EDGE_LOOP('',(#2569,#2570,#2571,#2572));
#1002=EDGE_LOOP('',(#2573));
#1166=CIRCLE('',#3469,0.5);
#1167=CIRCLE('',#3471,0.5);
#1168=CIRCLE('',#3473,0.5);
#1169=CIRCLE('',#3475,0.5);
#1170=CIRCLE('',#3477,0.5);
#1171=CIRCLE('',#3479,0.5);
#1172=CIRCLE('',#3481,0.5);
#1173=CIRCLE('',#3483,0.5);
#1174=CIRCLE('',#3485,0.5);
#1175=CIRCLE('',#3487,2.);
#1176=CIRCLE('',#3488,2.);
#1177=CIRCLE('',#3489,2.);
#1178=CIRCLE('',#3490,2.);
#1179=CIRCLE('',#3491,2.);
#1180=CIRCLE('',#3492,2.);
#1181=CIRCLE('',#3493,2.);
#1182=CIRCLE('',#3494,2.);
#1183=CIRCLE('',#3495,2.);
#1184=CIRCLE('',#3496,0.5);
#1185=CIRCLE('',#3497,2.);
#1186=CIRCLE('',#3498,1.);
#1187=CIRCLE('',#3500,2.);
#1188=CIRCLE('',#3502,2.);
#1189=CIRCLE('',#3504,2.);
#1190=CIRCLE('',#3506,2.);
#1191=CIRCLE('',#3508,2.);
#1192=CIRCLE('',#3510,2.);
#1193=CIRCLE('',#3512,2.);
#1194=CIRCLE('',#3514,2.);
#1195=CIRCLE('',#3516,2.);
#1196=CIRCLE('',#3518,1.5);
#1197=CIRCLE('',#3519,0.5);
#1198=CIRCLE('',#3520,2.);
#1199=CIRCLE('',#3525,1.);
#1409=VERTEX_POINT('',#5694);
#1410=VERTEX_POINT('',#5695);
#1411=VERTEX_POINT('',#5697);
#1412=VERTEX_POINT('',#5720);
#1413=VERTEX_POINT('',#5724);
#1414=VERTEX_POINT('',#5725);
#1415=VERTEX_POINT('',#5727);
#1416=VERTEX_POINT('',#5750);
#1417=VERTEX_POINT('',#5754);
#1418=VERTEX_POINT('',#5755);
#1419=VERTEX_POINT('',#5757);
#1420=VERTEX_POINT('',#5780);
#1421=VERTEX_POINT('',#5784);
#1422=VERTEX_POINT('',#5785);
#1423=VERTEX_POINT('',#5787);
#1424=VERTEX_POINT('',#5810);
#1425=VERTEX_POINT('',#5814);
#1426=VERTEX_POINT('',#5815);
#1427=VERTEX_POINT('',#5817);
#1428=VERTEX_POINT('',#5844);
#1429=VERTEX_POINT('',#5848);
#1430=VERTEX_POINT('',#5849);
#1431=VERTEX_POINT('',#5851);
#1432=VERTEX_POINT('',#5874);
#1433=VERTEX_POINT('',#5878);
#1434=VERTEX_POINT('',#5879);
#1435=VERTEX_POINT('',#5881);
#1436=VERTEX_POINT('',#5904);
#1437=VERTEX_POINT('',#5908);
#1438=VERTEX_POINT('',#5909);
#1439=VERTEX_POINT('',#5911);
#1440=VERTEX_POINT('',#5934);
#1441=VERTEX_POINT('',#5938);
#1442=VERTEX_POINT('',#5939);
#1443=VERTEX_POINT('',#5941);
#1444=VERTEX_POINT('',#5964);
#1445=VERTEX_POINT('',#5976);
#1446=VERTEX_POINT('',#5978);
#1447=VERTEX_POINT('',#5981);
#1448=VERTEX_POINT('',#5984);
#1449=VERTEX_POINT('',#6004);
#1450=VERTEX_POINT('',#6006);
#1451=VERTEX_POINT('',#6020);
#1452=VERTEX_POINT('',#6043);
#1787=EDGE_CURVE('',#1409,#1410,#291,.T.);
#1788=EDGE_CURVE('',#1411,#1409,#157,.T.);
#1789=EDGE_CURVE('',#1412,#1411,#292,.T.);
#1790=EDGE_CURVE('',#1410,#1412,#1166,.T.);
#1791=EDGE_CURVE('',#1413,#1414,#293,.T.);
#1792=EDGE_CURVE('',#1415,#1413,#158,.T.);
#1793=EDGE_CURVE('',#1416,#1415,#294,.T.);
#1794=EDGE_CURVE('',#1414,#1416,#1167,.T.);
#1795=EDGE_CURVE('',#1417,#1418,#295,.T.);
#1796=EDGE_CURVE('',#1419,#1417,#159,.T.);
#1797=EDGE_CURVE('',#1420,#1419,#296,.T.);
#1798=EDGE_CURVE('',#1418,#1420,#1168,.T.);
#1799=EDGE_CURVE('',#1421,#1422,#297,.T.);
#1800=EDGE_CURVE('',#1423,#1421,#160,.T.);
#1801=EDGE_CURVE('',#1424,#1423,#298,.T.);
#1802=EDGE_CURVE('',#1422,#1424,#1169,.T.);
#1803=EDGE_CURVE('',#1425,#1426,#299,.T.);
#1804=EDGE_CURVE('',#1427,#1425,#161,.T.);
#1805=EDGE_CURVE('',#1428,#1427,#300,.T.);
#1806=EDGE_CURVE('',#1426,#1428,#1170,.T.);
#1807=EDGE_CURVE('',#1429,#1430,#301,.T.);
#1808=EDGE_CURVE('',#1431,#1429,#162,.T.);
#1809=EDGE_CURVE('',#1432,#1431,#302,.T.);
#1810=EDGE_CURVE('',#1430,#1432,#1171,.T.);
#1811=EDGE_CURVE('',#1433,#1434,#303,.T.);
#1812=EDGE_CURVE('',#1435,#1433,#163,.T.);
#1813=EDGE_CURVE('',#1436,#1435,#304,.T.);
#1814=EDGE_CURVE('',#1434,#1436,#1172,.T.);
#1815=EDGE_CURVE('',#1437,#1438,#305,.T.);
#1816=EDGE_CURVE('',#1439,#1437,#164,.T.);
#1817=EDGE_CURVE('',#1440,#1439,#306,.T.);
#1818=EDGE_CURVE('',#1438,#1440,#1173,.T.);
#1819=EDGE_CURVE('',#1441,#1442,#307,.T.);
#1820=EDGE_CURVE('',#1443,#1441,#165,.T.);
#1821=EDGE_CURVE('',#1444,#1443,#308,.T.);
#1822=EDGE_CURVE('',#1442,#1444,#1174,.T.);
#1823=EDGE_CURVE('',#1414,#1412,#1175,.T.);
#1824=EDGE_CURVE('',#1418,#1416,#1176,.T.);
#1825=EDGE_CURVE('',#1422,#1420,#1177,.T.);
#1826=EDGE_CURVE('',#1426,#1424,#1178,.T.);
#1827=EDGE_CURVE('',#1430,#1428,#1179,.T.);
#1828=EDGE_CURVE('',#1434,#1432,#1180,.T.);
#1829=EDGE_CURVE('',#1438,#1436,#1181,.T.);
#1830=EDGE_CURVE('',#1442,#1440,#1182,.T.);
#1831=EDGE_CURVE('',#1445,#1444,#1183,.T.);
#1832=EDGE_CURVE('',#1445,#1446,#1184,.T.);
#1833=EDGE_CURVE('',#1410,#1446,#1185,.T.);
#1834=EDGE_CURVE('',#1447,#1447,#1186,.T.);
#1835=EDGE_CURVE('',#1448,#1443,#1187,.T.);
#1836=EDGE_CURVE('',#1448,#1445,#309,.T.);
#1837=EDGE_CURVE('',#1441,#1439,#1188,.T.);
#1838=EDGE_CURVE('',#1437,#1435,#1189,.T.);
#1839=EDGE_CURVE('',#1433,#1431,#1190,.T.);
#1840=EDGE_CURVE('',#1429,#1427,#1191,.T.);
#1841=EDGE_CURVE('',#1425,#1423,#1192,.T.);
#1842=EDGE_CURVE('',#1421,#1419,#1193,.T.);
#1843=EDGE_CURVE('',#1417,#1415,#1194,.T.);
#1844=EDGE_CURVE('',#1413,#1411,#1195,.T.);
#1845=EDGE_CURVE('',#1449,#1449,#1196,.T.);
#1846=EDGE_CURVE('',#1449,#1450,#1197,.T.);
#1847=EDGE_CURVE('',#1450,#1448,#166,.T.);
#1848=EDGE_CURVE('',#1409,#1451,#1198,.T.);
#1849=EDGE_CURVE('',#1451,#1450,#167,.T.);
#1850=EDGE_CURVE('',#1446,#1451,#310,.T.);
#1851=EDGE_CURVE('',#1452,#1452,#1199,.T.);
#1852=EDGE_CURVE('',#1452,#1447,#311,.T.);
#2442=ORIENTED_EDGE('',*,*,#1787,.F.);
#2443=ORIENTED_EDGE('',*,*,#1788,.F.);
#2444=ORIENTED_EDGE('',*,*,#1789,.F.);
#2445=ORIENTED_EDGE('',*,*,#1790,.F.);
#2446=ORIENTED_EDGE('',*,*,#1791,.F.);
#2447=ORIENTED_EDGE('',*,*,#1792,.F.);
#2448=ORIENTED_EDGE('',*,*,#1793,.F.);
#2449=ORIENTED_EDGE('',*,*,#1794,.F.);
#2450=ORIENTED_EDGE('',*,*,#1795,.F.);
#2451=ORIENTED_EDGE('',*,*,#1796,.F.);
#2452=ORIENTED_EDGE('',*,*,#1797,.F.);
#2453=ORIENTED_EDGE('',*,*,#1798,.F.);
#2454=ORIENTED_EDGE('',*,*,#1799,.F.);
#2455=ORIENTED_EDGE('',*,*,#1800,.F.);
#2456=ORIENTED_EDGE('',*,*,#1801,.F.);
#2457=ORIENTED_EDGE('',*,*,#1802,.F.);
#2458=ORIENTED_EDGE('',*,*,#1803,.F.);
#2459=ORIENTED_EDGE('',*,*,#1804,.F.);
#2460=ORIENTED_EDGE('',*,*,#1805,.F.);
#2461=ORIENTED_EDGE('',*,*,#1806,.F.);
#2462=ORIENTED_EDGE('',*,*,#1807,.F.);
#2463=ORIENTED_EDGE('',*,*,#1808,.F.);
#2464=ORIENTED_EDGE('',*,*,#1809,.F.);
#2465=ORIENTED_EDGE('',*,*,#1810,.F.);
#2466=ORIENTED_EDGE('',*,*,#1811,.F.);
#2467=ORIENTED_EDGE('',*,*,#1812,.F.);
#2468=ORIENTED_EDGE('',*,*,#1813,.F.);
#2469=ORIENTED_EDGE('',*,*,#1814,.F.);
#2470=ORIENTED_EDGE('',*,*,#1815,.F.);
#2471=ORIENTED_EDGE('',*,*,#1816,.F.);
#2472=ORIENTED_EDGE('',*,*,#1817,.F.);
#2473=ORIENTED_EDGE('',*,*,#1818,.F.);
#2474=ORIENTED_EDGE('',*,*,#1819,.F.);
#2475=ORIENTED_EDGE('',*,*,#1820,.F.);
#2476=ORIENTED_EDGE('',*,*,#1821,.F.);
#2477=ORIENTED_EDGE('',*,*,#1822,.F.);
#2478=ORIENTED_EDGE('',*,*,#1790,.T.);
#2479=ORIENTED_EDGE('',*,*,#1823,.F.);
#2480=ORIENTED_EDGE('',*,*,#1794,.T.);
#2481=ORIENTED_EDGE('',*,*,#1824,.F.);
#2482=ORIENTED_EDGE('',*,*,#1798,.T.);
#2483=ORIENTED_EDGE('',*,*,#1825,.F.);
#2484=ORIENTED_EDGE('',*,*,#1802,.T.);
#2485=ORIENTED_EDGE('',*,*,#1826,.F.);
#2486=ORIENTED_EDGE('',*,*,#1806,.T.);
#2487=ORIENTED_EDGE('',*,*,#1827,.F.);
#2488=ORIENTED_EDGE('',*,*,#1810,.T.);
#2489=ORIENTED_EDGE('',*,*,#1828,.F.);
#2490=ORIENTED_EDGE('',*,*,#1814,.T.);
#2491=ORIENTED_EDGE('',*,*,#1829,.F.);
#2492=ORIENTED_EDGE('',*,*,#1818,.T.);
#2493=ORIENTED_EDGE('',*,*,#1830,.F.);
#2494=ORIENTED_EDGE('',*,*,#1822,.T.);
#2495=ORIENTED_EDGE('',*,*,#1831,.F.);
#2496=ORIENTED_EDGE('',*,*,#1832,.T.);
#2497=ORIENTED_EDGE('',*,*,#1833,.F.);
#2498=ORIENTED_EDGE('',*,*,#1834,.T.);
#2499=ORIENTED_EDGE('',*,*,#1821,.T.);
#2500=ORIENTED_EDGE('',*,*,#1835,.F.);
#2501=ORIENTED_EDGE('',*,*,#1836,.T.);
#2502=ORIENTED_EDGE('',*,*,#1831,.T.);
#2503=ORIENTED_EDGE('',*,*,#1817,.T.);
#2504=ORIENTED_EDGE('',*,*,#1837,.F.);
#2505=ORIENTED_EDGE('',*,*,#1819,.T.);
#2506=ORIENTED_EDGE('',*,*,#1830,.T.);
#2507=ORIENTED_EDGE('',*,*,#1813,.T.);
#2508=ORIENTED_EDGE('',*,*,#1838,.F.);
#2509=ORIENTED_EDGE('',*,*,#1815,.T.);
#2510=ORIENTED_EDGE('',*,*,#1829,.T.);
#2511=ORIENTED_EDGE('',*,*,#1809,.T.);
#2512=ORIENTED_EDGE('',*,*,#1839,.F.);
#2513=ORIENTED_EDGE('',*,*,#1811,.T.);
#2514=ORIENTED_EDGE('',*,*,#1828,.T.);
#2515=ORIENTED_EDGE('',*,*,#1805,.T.);
#2516=ORIENTED_EDGE('',*,*,#1840,.F.);
#2517=ORIENTED_EDGE('',*,*,#1807,.T.);
#2518=ORIENTED_EDGE('',*,*,#1827,.T.);
#2519=ORIENTED_EDGE('',*,*,#1801,.T.);
#2520=ORIENTED_EDGE('',*,*,#1841,.F.);
#2521=ORIENTED_EDGE('',*,*,#1803,.T.);
#2522=ORIENTED_EDGE('',*,*,#1826,.T.);
#2523=ORIENTED_EDGE('',*,*,#1797,.T.);
#2524=ORIENTED_EDGE('',*,*,#1842,.F.);
#2525=ORIENTED_EDGE('',*,*,#1799,.T.);
#2526=ORIENTED_EDGE('',*,*,#1825,.T.);
#2527=ORIENTED_EDGE('',*,*,#1793,.T.);
#2528=ORIENTED_EDGE('',*,*,#1843,.F.);
#2529=ORIENTED_EDGE('',*,*,#1795,.T.);
#2530=ORIENTED_EDGE('',*,*,#1824,.T.);
#2531=ORIENTED_EDGE('',*,*,#1789,.T.);
#2532=ORIENTED_EDGE('',*,*,#1844,.F.);
#2533=ORIENTED_EDGE('',*,*,#1791,.T.);
#2534=ORIENTED_EDGE('',*,*,#1823,.T.);
#2535=ORIENTED_EDGE('',*,*,#1845,.T.);
#2536=ORIENTED_EDGE('',*,*,#1846,.T.);
#2537=ORIENTED_EDGE('',*,*,#1847,.T.);
#2538=ORIENTED_EDGE('',*,*,#1835,.T.);
#2539=ORIENTED_EDGE('',*,*,#1820,.T.);
#2540=ORIENTED_EDGE('',*,*,#1837,.T.);
#2541=ORIENTED_EDGE('',*,*,#1816,.T.);
#2542=ORIENTED_EDGE('',*,*,#1838,.T.);
#2543=ORIENTED_EDGE('',*,*,#1812,.T.);
#2544=ORIENTED_EDGE('',*,*,#1839,.T.);
#2545=ORIENTED_EDGE('',*,*,#1808,.T.);
#2546=ORIENTED_EDGE('',*,*,#1840,.T.);
#2547=ORIENTED_EDGE('',*,*,#1804,.T.);
#2548=ORIENTED_EDGE('',*,*,#1841,.T.);
#2549=ORIENTED_EDGE('',*,*,#1800,.T.);
#2550=ORIENTED_EDGE('',*,*,#1842,.T.);
#2551=ORIENTED_EDGE('',*,*,#1796,.T.);
#2552=ORIENTED_EDGE('',*,*,#1843,.T.);
#2553=ORIENTED_EDGE('',*,*,#1792,.T.);
#2554=ORIENTED_EDGE('',*,*,#1844,.T.);
#2555=ORIENTED_EDGE('',*,*,#1788,.T.);
#2556=ORIENTED_EDGE('',*,*,#1848,.T.);
#2557=ORIENTED_EDGE('',*,*,#1849,.T.);
#2558=ORIENTED_EDGE('',*,*,#1846,.F.);
#2559=ORIENTED_EDGE('',*,*,#1836,.F.);
#2560=ORIENTED_EDGE('',*,*,#1847,.F.);
#2561=ORIENTED_EDGE('',*,*,#1849,.F.);
#2562=ORIENTED_EDGE('',*,*,#1850,.F.);
#2563=ORIENTED_EDGE('',*,*,#1832,.F.);
#2564=ORIENTED_EDGE('',*,*,#1787,.T.);
#2565=ORIENTED_EDGE('',*,*,#1833,.T.);
#2566=ORIENTED_EDGE('',*,*,#1850,.T.);
#2567=ORIENTED_EDGE('',*,*,#1848,.F.);
#2568=ORIENTED_EDGE('',*,*,#1845,.F.);
#2569=ORIENTED_EDGE('',*,*,#1851,.F.);
#2570=ORIENTED_EDGE('',*,*,#1852,.T.);
#2571=ORIENTED_EDGE('',*,*,#1834,.F.);
#2572=ORIENTED_EDGE('',*,*,#1852,.F.);
#2573=ORIENTED_EDGE('',*,*,#1851,.T.);
#3029=TOROIDAL_SURFACE('',#3517,1.5,0.5);
#3098=ADVANCED_FACE('',(#794),#603,.F.);
#3099=ADVANCED_FACE('',(#795),#604,.F.);
#3100=ADVANCED_FACE('',(#796),#605,.F.);
#3101=ADVANCED_FACE('',(#797),#606,.F.);
#3102=ADVANCED_FACE('',(#798),#607,.F.);
#3103=ADVANCED_FACE('',(#799),#608,.F.);
#3104=ADVANCED_FACE('',(#800),#609,.F.);
#3105=ADVANCED_FACE('',(#801),#610,.F.);
#3106=ADVANCED_FACE('',(#802),#611,.F.);
#3107=ADVANCED_FACE('',(#803,#690),#707,.F.);
#3108=ADVANCED_FACE('',(#804),#612,.T.);
#3109=ADVANCED_FACE('',(#805),#613,.T.);
#3110=ADVANCED_FACE('',(#806),#614,.T.);
#3111=ADVANCED_FACE('',(#807),#615,.T.);
#3112=ADVANCED_FACE('',(#808),#616,.T.);
#3113=ADVANCED_FACE('',(#809),#617,.T.);
#3114=ADVANCED_FACE('',(#810),#618,.T.);
#3115=ADVANCED_FACE('',(#811),#619,.T.);
#3116=ADVANCED_FACE('',(#812),#620,.T.);
#3117=ADVANCED_FACE('',(#813),#3029,.T.);
#3118=ADVANCED_FACE('',(#814),#621,.F.);
#3119=ADVANCED_FACE('',(#815),#622,.T.);
#3120=ADVANCED_FACE('',(#816),#708,.T.);
#3121=ADVANCED_FACE('',(#817),#623,.T.);
#3122=ADVANCED_FACE('',(#818),#709,.F.);
#3216=CLOSED_SHELL('',(#3098,#3099,#3100,#3101,#3102,#3103,#3104,#3105,
#3106,#3107,#3108,#3109,#3110,#3111,#3112,#3113,#3114,#3115,#3116,#3117,
#3118,#3119,#3120,#3121,#3122));
#3467=AXIS2_PLACEMENT_3D('',#5692,#4050,#4051);
#3468=AXIS2_PLACEMENT_3D('',#5693,#4052,#4053);
#3469=AXIS2_PLACEMENT_3D('',#5722,#4056,#4057);
#3470=AXIS2_PLACEMENT_3D('',#5723,#4058,#4059);
#3471=AXIS2_PLACEMENT_3D('',#5752,#4062,#4063);
#3472=AXIS2_PLACEMENT_3D('',#5753,#4064,#4065);
#3473=AXIS2_PLACEMENT_3D('',#5782,#4068,#4069);
#3474=AXIS2_PLACEMENT_3D('',#5783,#4070,#4071);
#3475=AXIS2_PLACEMENT_3D('',#5812,#4074,#4075);
#3476=AXIS2_PLACEMENT_3D('',#5813,#4076,#4077);
#3477=AXIS2_PLACEMENT_3D('',#5846,#4080,#4081);
#3478=AXIS2_PLACEMENT_3D('',#5847,#4082,#4083);
#3479=AXIS2_PLACEMENT_3D('',#5876,#4086,#4087);
#3480=AXIS2_PLACEMENT_3D('',#5877,#4088,#4089);
#3481=AXIS2_PLACEMENT_3D('',#5906,#4092,#4093);
#3482=AXIS2_PLACEMENT_3D('',#5907,#4094,#4095);
#3483=AXIS2_PLACEMENT_3D('',#5936,#4098,#4099);
#3484=AXIS2_PLACEMENT_3D('',#5937,#4100,#4101);
#3485=AXIS2_PLACEMENT_3D('',#5966,#4104,#4105);
#3486=AXIS2_PLACEMENT_3D('',#5967,#4106,#4107);
#3487=AXIS2_PLACEMENT_3D('',#5968,#4108,#4109);
#3488=AXIS2_PLACEMENT_3D('',#5969,#4110,#4111);
#3489=AXIS2_PLACEMENT_3D('',#5970,#4112,#4113);
#3490=AXIS2_PLACEMENT_3D('',#5971,#4114,#4115);
#3491=AXIS2_PLACEMENT_3D('',#5972,#4116,#4117);
#3492=AXIS2_PLACEMENT_3D('',#5973,#4118,#4119);
#3493=AXIS2_PLACEMENT_3D('',#5974,#4120,#4121);
#3494=AXIS2_PLACEMENT_3D('',#5975,#4122,#4123);
#3495=AXIS2_PLACEMENT_3D('',#5977,#4124,#4125);
#3496=AXIS2_PLACEMENT_3D('',#5979,#4126,#4127);
#3497=AXIS2_PLACEMENT_3D('',#5980,#4128,#4129);
#3498=AXIS2_PLACEMENT_3D('',#5982,#4130,#4131);
#3499=AXIS2_PLACEMENT_3D('',#5983,#4132,#4133);
#3500=AXIS2_PLACEMENT_3D('',#5985,#4134,#4135);
#3501=AXIS2_PLACEMENT_3D('',#5987,#4137,#4138);
#3502=AXIS2_PLACEMENT_3D('',#5988,#4139,#4140);
#3503=AXIS2_PLACEMENT_3D('',#5989,#4141,#4142);
#3504=AXIS2_PLACEMENT_3D('',#5990,#4143,#4144);
#3505=AXIS2_PLACEMENT_3D('',#5991,#4145,#4146);
#3506=AXIS2_PLACEMENT_3D('',#5992,#4147,#4148);
#3507=AXIS2_PLACEMENT_3D('',#5993,#4149,#4150);
#3508=AXIS2_PLACEMENT_3D('',#5994,#4151,#4152);
#3509=AXIS2_PLACEMENT_3D('',#5995,#4153,#4154);
#3510=AXIS2_PLACEMENT_3D('',#5996,#4155,#4156);
#3511=AXIS2_PLACEMENT_3D('',#5997,#4157,#4158);
#3512=AXIS2_PLACEMENT_3D('',#5998,#4159,#4160);
#3513=AXIS2_PLACEMENT_3D('',#5999,#4161,#4162);
#3514=AXIS2_PLACEMENT_3D('',#6000,#4163,#4164);
#3515=AXIS2_PLACEMENT_3D('',#6001,#4165,#4166);
#3516=AXIS2_PLACEMENT_3D('',#6002,#4167,#4168);
#3517=AXIS2_PLACEMENT_3D('',#6003,#4169,#4170);
#3518=AXIS2_PLACEMENT_3D('',#6005,#4171,#4172);
#3519=AXIS2_PLACEMENT_3D('',#6007,#4173,#4174);
#3520=AXIS2_PLACEMENT_3D('',#6021,#4175,#4176);
#3521=AXIS2_PLACEMENT_3D('',#6038,#4177,#4178);
#3522=AXIS2_PLACEMENT_3D('',#6040,#4180,#4181);
#3523=AXIS2_PLACEMENT_3D('',#6041,#4182,#4183);
#3524=AXIS2_PLACEMENT_3D('',#6042,#4184,#4185);
#3525=AXIS2_PLACEMENT_3D('',#6044,#4186,#4187);
#3526=AXIS2_PLACEMENT_3D('',#6046,#4189,#4190);
#4050=DIRECTION('axis',(0.,0.,1.));
#4051=DIRECTION('refdir',(1.,0.,0.));
#4052=DIRECTION('center_axis',(0.,0.,-1.));
#4053=DIRECTION('ref_axis',(0.809016994374947,-0.587785252292473,0.));
#4054=DIRECTION('',(0.,0.,-1.));
#4055=DIRECTION('',(0.,0.,1.));
#4056=DIRECTION('center_axis',(0.,0.,1.));
#4057=DIRECTION('ref_axis',(-0.809016994374947,0.587785252292473,0.));
#4058=DIRECTION('center_axis',(0.,0.,-1.));
#4059=DIRECTION('ref_axis',(0.309016994374946,-0.951056516295154,0.));
#4060=DIRECTION('',(0.,0.,-1.));
#4061=DIRECTION('',(0.,0.,1.));
#4062=DIRECTION('center_axis',(0.,0.,1.));
#4063=DIRECTION('ref_axis',(-0.309016994374947,0.951056516295154,0.));
#4064=DIRECTION('center_axis',(0.,0.,-1.));
#4065=DIRECTION('ref_axis',(-0.309016994374949,-0.951056516295153,0.));
#4066=DIRECTION('',(0.,0.,-1.));
#4067=DIRECTION('',(0.,0.,1.));
#4068=DIRECTION('center_axis',(0.,0.,1.));
#4069=DIRECTION('ref_axis',(0.309016994374948,0.951056516295154,0.));
#4070=DIRECTION('center_axis',(0.,0.,-1.));
#4071=DIRECTION('ref_axis',(-0.809016994374947,-0.587785252292474,0.));
#4072=DIRECTION('',(0.,0.,-1.));
#4073=DIRECTION('',(0.,0.,1.));
#4074=DIRECTION('center_axis',(0.,0.,1.));
#4075=DIRECTION('ref_axis',(0.809016994374947,0.587785252292473,0.));
#4076=DIRECTION('center_axis',(0.,0.,-1.));
#4077=DIRECTION('ref_axis',(-1.,2.6124255799288E-16,0.));
#4078=DIRECTION('',(0.,0.,-1.));
#4079=DIRECTION('',(0.,0.,1.));
#4080=DIRECTION('center_axis',(0.,0.,1.));
#4081=DIRECTION('ref_axis',(1.,-1.38777878078144E-16,0.));
#4082=DIRECTION('center_axis',(0.,0.,-1.));
#4083=DIRECTION('ref_axis',(-0.809016994374947,0.587785252292473,0.));
#4084=DIRECTION('',(0.,0.,-1.));
#4085=DIRECTION('',(0.,0.,1.));
#4086=DIRECTION('center_axis',(0.,0.,1.));
#4087=DIRECTION('ref_axis',(0.809016994374947,-0.587785252292473,0.));
#4088=DIRECTION('center_axis',(0.,0.,-1.));
#4089=DIRECTION('ref_axis',(-0.309016994374946,0.951056516295154,0.));
#4090=DIRECTION('',(0.,0.,-1.));
#4091=DIRECTION('',(0.,0.,1.));
#4092=DIRECTION('center_axis',(0.,0.,1.));
#4093=DIRECTION('ref_axis',(0.309016994374947,-0.951056516295154,0.));
#4094=DIRECTION('center_axis',(0.,0.,-1.));
#4095=DIRECTION('ref_axis',(0.309016994374946,0.951056516295154,0.));
#4096=DIRECTION('',(0.,0.,-1.));
#4097=DIRECTION('',(0.,0.,1.));
#4098=DIRECTION('center_axis',(0.,0.,1.));
#4099=DIRECTION('ref_axis',(-0.309016994374947,-0.951056516295154,0.));
#4100=DIRECTION('center_axis',(0.,0.,-1.));
#4101=DIRECTION('ref_axis',(0.809016994374947,0.587785252292474,0.));
#4102=DIRECTION('',(0.,0.,-1.));
#4103=DIRECTION('',(0.,0.,1.));
#4104=DIRECTION('center_axis',(0.,0.,1.));
#4105=DIRECTION('ref_axis',(-0.809016994374947,-0.587785252292473,0.));
#4106=DIRECTION('center_axis',(0.,0.,1.));
#4107=DIRECTION('ref_axis',(1.,0.,0.));
#4108=DIRECTION('center_axis',(0.,0.,1.));
#4109=DIRECTION('ref_axis',(1.,0.,0.));
#4110=DIRECTION('center_axis',(0.,0.,1.));
#4111=DIRECTION('ref_axis',(1.,0.,0.));
#4112=DIRECTION('center_axis',(0.,0.,1.));
#4113=DIRECTION('ref_axis',(1.,0.,0.));
#4114=DIRECTION('center_axis',(0.,0.,1.));
#4115=DIRECTION('ref_axis',(1.,0.,0.));
#4116=DIRECTION('center_axis',(0.,0.,1.));
#4117=DIRECTION('ref_axis',(1.,0.,0.));
#4118=DIRECTION('center_axis',(0.,0.,1.));
#4119=DIRECTION('ref_axis',(1.,0.,0.));
#4120=DIRECTION('center_axis',(0.,0.,1.));
#4121=DIRECTION('ref_axis',(1.,0.,0.));
#4122=DIRECTION('center_axis',(0.,0.,1.));
#4123=DIRECTION('ref_axis',(1.,0.,0.));
#4124=DIRECTION('center_axis',(0.,0.,1.));
#4125=DIRECTION('ref_axis',(1.,0.,0.));
#4126=DIRECTION('center_axis',(0.,0.,1.));
#4127=DIRECTION('ref_axis',(-1.,0.,0.));
#4128=DIRECTION('center_axis',(0.,0.,1.));
#4129=DIRECTION('ref_axis',(1.,0.,0.));
#4130=DIRECTION('center_axis',(0.,0.,1.));
#4131=DIRECTION('ref_axis',(1.,0.,0.));
#4132=DIRECTION('center_axis',(0.,0.,1.));
#4133=DIRECTION('ref_axis',(1.,0.,0.));
#4134=DIRECTION('center_axis',(0.,0.,1.));
#4135=DIRECTION('ref_axis',(1.,0.,0.));
#4136=DIRECTION('',(0.,0.,-1.));
#4137=DIRECTION('center_axis',(0.,0.,1.));
#4138=DIRECTION('ref_axis',(1.,0.,0.));
#4139=DIRECTION('center_axis',(0.,0.,1.));
#4140=DIRECTION('ref_axis',(1.,0.,0.));
#4141=DIRECTION('center_axis',(0.,0.,1.));
#4142=DIRECTION('ref_axis',(1.,0.,0.));
#4143=DIRECTION('center_axis',(0.,0.,1.));
#4144=DIRECTION('ref_axis',(1.,0.,0.));
#4145=DIRECTION('center_axis',(0.,0.,1.));
#4146=DIRECTION('ref_axis',(1.,0.,0.));
#4147=DIRECTION('center_axis',(0.,0.,1.));
#4148=DIRECTION('ref_axis',(1.,0.,0.));
#4149=DIRECTION('center_axis',(0.,0.,1.));
#4150=DIRECTION('ref_axis',(1.,0.,0.));
#4151=DIRECTION('center_axis',(0.,0.,1.));
#4152=DIRECTION('ref_axis',(1.,0.,0.));
#4153=DIRECTION('center_axis',(0.,0.,1.));
#4154=DIRECTION('ref_axis',(1.,0.,0.));
#4155=DIRECTION('center_axis',(0.,0.,1.));
#4156=DIRECTION('ref_axis',(1.,0.,0.));
#4157=DIRECTION('center_axis',(0.,0.,1.));
#4158=DIRECTION('ref_axis',(1.,0.,0.));
#4159=DIRECTION('center_axis',(0.,0.,1.));
#4160=DIRECTION('ref_axis',(1.,0.,0.));
#4161=DIRECTION('center_axis',(0.,0.,1.));
#4162=DIRECTION('ref_axis',(1.,0.,0.));
#4163=DIRECTION('center_axis',(0.,0.,1.));
#4164=DIRECTION('ref_axis',(1.,0.,0.));
#4165=DIRECTION('center_axis',(0.,0.,1.));
#4166=DIRECTION('ref_axis',(1.,0.,0.));
#4167=DIRECTION('center_axis',(0.,0.,1.));
#4168=DIRECTION('ref_axis',(1.,0.,0.));
#4169=DIRECTION('center_axis',(0.,0.,1.));
#4170=DIRECTION('ref_axis',(1.,0.,0.));
#4171=DIRECTION('center_axis',(0.,0.,-1.));
#4172=DIRECTION('ref_axis',(1.,0.,0.));
#4173=DIRECTION('center_axis',(1.22464679914735E-16,-1.,0.));
#4174=DIRECTION('ref_axis',(-1.,-1.22464679914735E-16,0.));
#4175=DIRECTION('center_axis',(0.,0.,1.));
#4176=DIRECTION('ref_axis',(1.,0.,0.));
#4177=DIRECTION('center_axis',(0.,0.,-1.));
#4178=DIRECTION('ref_axis',(1.,-1.22464679914735E-16,0.));
#4179=DIRECTION('',(0.,0.,1.));
#4180=DIRECTION('center_axis',(0.,0.,1.));
#4181=DIRECTION('ref_axis',(1.,0.,0.));
#4182=DIRECTION('center_axis',(0.,0.,1.));
#4183=DIRECTION('ref_axis',(1.,0.,0.));
#4184=DIRECTION('center_axis',(0.,0.,-1.));
#4185=DIRECTION('ref_axis',(1.,0.,0.));
#4186=DIRECTION('center_axis',(0.,0.,-1.));
#4187=DIRECTION('ref_axis',(1.,0.,0.));
#4188=DIRECTION('',(0.,0.,1.));
#4189=DIRECTION('center_axis',(0.,0.,1.));
#4190=DIRECTION('ref_axis',(1.,0.,0.));
#5692=CARTESIAN_POINT('',(0.,0.,0.));
#5693=CARTESIAN_POINT('Origin',(10.9788681304862,1.34514335437282,16.));
#5694=CARTESIAN_POINT('',(11.0183695787139,0.846706161149926,15.5));
#5695=CARTESIAN_POINT('',(11.0183695787139,0.846706161149926,12.));
#5696=CARTESIAN_POINT('',(11.0183695787139,0.846706161149926,16.));
#5697=CARTESIAN_POINT('',(11.4651166898695,1.46160080796717,15.5));
#5698=CARTESIAN_POINT('Ctrl Pts',(11.4651166898695,1.46160080796717,15.5));
#5699=CARTESIAN_POINT('Ctrl Pts',(11.4651166898695,1.46160080796717,15.5327258400527));
#5700=CARTESIAN_POINT('Ctrl Pts',(11.4660168040712,1.45801754115624,15.5654293765226));
#5701=CARTESIAN_POINT('Ctrl Pts',(11.4691283383932,1.44362639892173,15.6290406866894));
#5702=CARTESIAN_POINT('Ctrl Pts',(11.4713273005329,1.43286974240523,15.6598442001575));
#5703=CARTESIAN_POINT('Ctrl Pts',(11.4765149298,1.39787805797502,15.7305775282065));
#5704=CARTESIAN_POINT('Ctrl Pts',(11.4793990336829,1.37028664210651,15.7678051908843));
#5705=CARTESIAN_POINT('Ctrl Pts',(11.4782015086689,1.30346706538635,15.8295297239576));
#5706=CARTESIAN_POINT('Ctrl Pts',(11.4743049792552,1.26629507509822,15.853094168515));
#5707=CARTESIAN_POINT('Ctrl Pts',(11.4549023017239,1.18683333243691,15.8881049113845));
#5708=CARTESIAN_POINT('Ctrl Pts',(11.4397065054753,1.14620200545152,15.8989286877205));
#5709=CARTESIAN_POINT('Ctrl Pts',(11.396404023885,1.06610334829151,15.9101071881998));
#5710=CARTESIAN_POINT('Ctrl Pts',(11.3678139645159,1.02747859678379,15.909753701168));
#5711=CARTESIAN_POINT('Ctrl Pts',(11.302566216258,0.961281878811867,15.8967861544805));
#5712=CARTESIAN_POINT('Ctrl Pts',(11.2665927725368,0.934059884456842,15.8843843767206));
#5713=CARTESIAN_POINT('Ctrl Pts',(11.1952176199532,0.89256475492642,15.8454873880819));
#5714=CARTESIAN_POINT('Ctrl Pts',(11.1614633805605,0.878606603360417,15.8203384131985));
#5715=CARTESIAN_POINT('Ctrl Pts',(11.0976617200424,0.858171109417801,15.7531662441803));
#5716=CARTESIAN_POINT('Ctrl Pts',(11.0703452620001,0.85319590461791,15.7112656542922));
#5717=CARTESIAN_POINT('Ctrl Pts',(11.0294097048913,0.84722400890498,15.6129130718351));
#5718=CARTESIAN_POINT('Ctrl Pts',(11.0183695787139,0.846706161149926,15.5565891907874));
#5719=CARTESIAN_POINT('Ctrl Pts',(11.0183695787139,0.846706161149926,15.5));
#5720=CARTESIAN_POINT('',(11.4651166898695,1.46160080796717,12.));
#5721=CARTESIAN_POINT('',(11.4651166898695,1.46160080796717,16.));
#5722=CARTESIAN_POINT('Origin',(10.9788681304862,1.34514335437282,12.));
#5723=CARTESIAN_POINT('Origin',(12.1231154122328,2.17648766711626,16.));
#5724=CARTESIAN_POINT('',(11.862098723781,1.75002513845795,15.5));
#5725=CARTESIAN_POINT('',(11.862098723781,1.75002513845795,12.));
#5726=CARTESIAN_POINT('',(11.862098723781,1.75002513845795,16.));
#5727=CARTESIAN_POINT('',(12.5849507340066,1.98489399404177,15.5));
#5728=CARTESIAN_POINT('Ctrl Pts',(12.5849507340066,1.98489399404177,15.5));
#5729=CARTESIAN_POINT('Ctrl Pts',(12.5849507340066,1.98489399404177,15.5315974346976));
#5730=CARTESIAN_POINT('Ctrl Pts',(12.5836637760388,1.98169929993151,15.5631757175052));
#5731=CARTESIAN_POINT('Ctrl Pts',(12.5781379778504,1.96911950577423,15.6247606509986));
#5732=CARTESIAN_POINT('Ctrl Pts',(12.5739120210771,1.9597668107847,15.6546762688613));
#5733=CARTESIAN_POINT('Ctrl Pts',(12.5584805763086,1.92978725799424,15.7249493973573));
#5734=CARTESIAN_POINT('Ctrl Pts',(12.5451313949437,1.906259901776,15.762620760625));
#5735=CARTESIAN_POINT('Ctrl Pts',(12.5060588179609,1.85338430197355,15.8255830998499));
#5736=CARTESIAN_POINT('Ctrl Pts',(12.4815883321467,1.82554632233921,15.8498680529139));
#5737=CARTESIAN_POINT('Ctrl Pts',(12.4192606585594,1.77146870244053,15.8866893895236));
#5738=CARTESIAN_POINT('Ctrl Pts',(12.382396883207,1.74656759203559,15.8982106592639));
#5739=CARTESIAN_POINT('Ctrl Pts',(12.2978763951411,1.70550952857365,15.9102329913456));
#5740=CARTESIAN_POINT('Ctrl Pts',(12.2502943035319,1.69050766300347,15.909874133055));
#5741=CARTESIAN_POINT('Ctrl Pts',(12.1579952361435,1.67568037378513,15.8963684971709));
#5742=CARTESIAN_POINT('Ctrl Pts',(12.1140332395114,1.67487990467903,15.8841705706778));
#5743=CARTESIAN_POINT('Ctrl Pts',(12.032581997837,1.68306934122621,15.8458060158298));
#5744=CARTESIAN_POINT('Ctrl Pts',(11.9968182859843,1.69165869793162,15.8205491017219));
#5745=CARTESIAN_POINT('Ctrl Pts',(11.9330125310872,1.71268387513612,15.7531986669259));
#5746=CARTESIAN_POINT('Ctrl Pts',(11.9079924325872,1.7247105935723,15.7113185385228));
#5747=CARTESIAN_POINT('Ctrl Pts',(11.8713435677214,1.74394867728652,15.6129675013504));
#5748=CARTESIAN_POINT('Ctrl Pts',(11.862098723781,1.75002513845795,15.5566167040035));
#5749=CARTESIAN_POINT('Ctrl Pts',(11.862098723781,1.75002513845795,15.5));
#5750=CARTESIAN_POINT('',(12.5849507340066,1.98489399404177,12.));
#5751=CARTESIAN_POINT('',(12.5849507340066,1.98489399404177,16.));
#5752=CARTESIAN_POINT('Origin',(12.1231154122328,2.17648766711626,12.));
#5753=CARTESIAN_POINT('Origin',(13.537482835541,2.17648766711626,16.));
#5754=CARTESIAN_POINT('',(13.0756475137673,1.98489399404177,15.5));
#5755=CARTESIAN_POINT('',(13.0756475137673,1.98489399404177,12.));
#5756=CARTESIAN_POINT('',(13.0756475137673,1.98489399404177,16.));
#5757=CARTESIAN_POINT('',(13.7984995239928,1.75002513845795,15.5));
#5758=CARTESIAN_POINT('Ctrl Pts',(13.7984995239928,1.75002513845795,15.5));
#5759=CARTESIAN_POINT('Ctrl Pts',(13.7984995239928,1.75002513845795,15.5315974346976));
#5760=CARTESIAN_POINT('Ctrl Pts',(13.7955805590423,1.74819703154467,15.5631757175052));
#5761=CARTESIAN_POINT('Ctrl Pts',(13.7837158769179,1.74126774696798,15.6247606509986));
#5762=CARTESIAN_POINT('Ctrl Pts',(13.7747996298867,1.73618521284642,15.6546762688613));
#5763=CARTESIAN_POINT('Ctrl Pts',(13.7446937898207,1.72100162081168,15.7249493973573));
#5764=CARTESIAN_POINT('Ctrl Pts',(13.7200650422249,1.70981404173489,15.762620760625));
#5765=CARTESIAN_POINT('Ctrl Pts',(13.6573751656619,1.69000306742646,15.8255830998499));
#5766=CARTESIAN_POINT('Ctrl Pts',(13.6212153728949,1.68186505949125,15.8498680529139));
#5767=CARTESIAN_POINT('Ctrl Pts',(13.5390051982874,1.67475063332216,15.8866893895236));
#5768=CARTESIAN_POINT('Ctrl Pts',(13.4945452720888,1.67627319532172,15.8982106592639));
#5769=CARTESIAN_POINT('Ctrl Pts',(13.40203343668,1.69273642062657,15.9102329913456));
#5770=CARTESIAN_POINT('Ctrl Pts',(13.3547208406011,1.70856770815414,15.909874133055));
#5771=CARTESIAN_POINT('Ctrl Pts',(13.271334064585,1.7508242098072,15.8963684971709));
#5772=CARTESIAN_POINT('Ctrl Pts',(13.2352975582675,1.77601682997859,15.8841705706778));
#5773=CARTESIAN_POINT('Ctrl Pts',(13.174215749567,1.83051806195672,15.8458060158298));
#5774=CARTESIAN_POINT('Ctrl Pts',(13.1503309960943,1.85848837989641,15.8205491017219));
#5775=CARTESIAN_POINT('Ctrl Pts',(13.1110693451313,1.91300218730451,15.7531986669259));
#5776=CARTESIAN_POINT('Ctrl Pts',(13.0978967879741,1.93743845181515,15.7113185385228));
#5777=CARTESIAN_POINT('Ctrl Pts',(13.0795550953627,1.97454405076051,15.6129675013504));
#5778=CARTESIAN_POINT('Ctrl Pts',(13.0756475137673,1.98489399404177,15.5566167040035));
#5779=CARTESIAN_POINT('Ctrl Pts',(13.0756475137673,1.98489399404177,15.5));
#5780=CARTESIAN_POINT('',(13.7984995239928,1.75002513845795,12.));
#5781=CARTESIAN_POINT('',(13.7984995239928,1.75002513845795,16.));
#5782=CARTESIAN_POINT('Origin',(13.537482835541,2.17648766711626,12.));
#5783=CARTESIAN_POINT('Origin',(14.6817301172876,1.34514335437282,16.));
#5784=CARTESIAN_POINT('',(14.1954815579043,1.46160080796717,15.5));
#5785=CARTESIAN_POINT('',(14.1954815579043,1.46160080796717,12.));
#5786=CARTESIAN_POINT('',(14.1954815579043,1.46160080796717,16.));
#5787=CARTESIAN_POINT('',(14.6422286690599,0.846706161149931,15.5));
#5788=CARTESIAN_POINT('Ctrl Pts',(14.6422286690599,0.84670616114993,15.5));
#5789=CARTESIAN_POINT('Ctrl Pts',(14.6422286690599,0.84670616114993,15.5328840768056));
#5790=CARTESIAN_POINT('Ctrl Pts',(14.6385068660889,0.846959432552971,15.5657453762427));
#5791=CARTESIAN_POINT('Ctrl Pts',(14.6237151505491,0.848465062627269,15.6296563210017));
#5792=CARTESIAN_POINT('Ctrl Pts',(14.6126966763369,0.849713657088164,15.660598638283));
#5793=CARTESIAN_POINT('Ctrl Pts',(14.5776079356378,0.855659177572526,15.7313318911412));
#5794=CARTESIAN_POINT('Ctrl Pts',(14.550441321518,0.861482780240192,15.7684373555081));
#5795=CARTESIAN_POINT('Ctrl Pts',(14.4872412940069,0.883356517365064,15.8299542128302));
#5796=CARTESIAN_POINT('Ctrl Pts',(14.4530989465518,0.898598843657317,15.8534299122416));
#5797=CARTESIAN_POINT('Ctrl Pts',(14.3835813171714,0.941686180099718,15.8882855843752));
#5798=CARTESIAN_POINT('Ctrl Pts',(14.3496795039836,0.968726370854913,15.89904798654));
#5799=CARTESIAN_POINT('Ctrl Pts',(14.2869736205215,1.03471311698917,15.9101249054252));
#5800=CARTESIAN_POINT('Ctrl Pts',(14.2591225164167,1.07386600486173,15.9097261007587));
#5801=CARTESIAN_POINT('Ctrl Pts',(14.2165374803957,1.15619086111778,15.8966960156851));
#5802=CARTESIAN_POINT('Ctrl Pts',(14.201856352804,1.19858800968841,15.8843371675477));
#5803=CARTESIAN_POINT('Ctrl Pts',(14.1844547128968,1.27913917972905,15.8455544418483));
#5804=CARTESIAN_POINT('Ctrl Pts',(14.1816023263936,1.31560737922412,15.8203829360199));
#5805=CARTESIAN_POINT('Ctrl Pts',(14.1818824447642,1.38264039078621,15.7531735756887));
#5806=CARTESIAN_POINT('Ctrl Pts',(14.1855913480644,1.41015640885706,15.7112772176026));
#5807=CARTESIAN_POINT('Ctrl Pts',(14.1925617954654,1.4509387910301,15.6129247586851));
#5808=CARTESIAN_POINT('Ctrl Pts',(14.1954815579043,1.46160080796717,15.5565950982509));
#5809=CARTESIAN_POINT('Ctrl Pts',(14.1954815579043,1.46160080796717,15.5));
#5810=CARTESIAN_POINT('',(14.6422286690599,0.846706161149931,12.));
#5811=CARTESIAN_POINT('',(14.6422286690599,0.84670616114993,16.));
#5812=CARTESIAN_POINT('Origin',(14.6817301172876,1.34514335437282,12.));
#5813=CARTESIAN_POINT('Origin',(15.1187936873802,2.22044604925031E-15,16.));
#5814=CARTESIAN_POINT('',(14.793862313091,0.380025791233419,15.5));
#5815=CARTESIAN_POINT('',(14.793862313091,0.380025791233419,12.));
#5816=CARTESIAN_POINT('',(14.793862313091,0.380025791233419,16.));
#5817=CARTESIAN_POINT('',(14.793862313091,-0.380025791233415,15.5));
#5818=CARTESIAN_POINT('Ctrl Pts',(14.793862313091,-0.380025791233415,15.5));
#5819=CARTESIAN_POINT('Ctrl Pts',(14.793862313091,-0.380025791233415,15.5301189378802));
#5820=CARTESIAN_POINT('Ctrl Pts',(14.7914649109341,-0.378014471067455,15.5602222957306));
#5821=CARTESIAN_POINT('Ctrl Pts',(14.7820629540924,-0.369665255070382,15.619473583796));
#5822=CARTESIAN_POINT('Ctrl Pts',(14.7750166556806,-0.363286881363678,15.6485271997616));
#5823=CARTESIAN_POINT('Ctrl Pts',(14.7530701481314,-0.341440768177844,15.7162986234851));
#5824=CARTESIAN_POINT('Ctrl Pts',(14.736260482547,-0.323422662348315,15.7528086416089));
#5825=CARTESIAN_POINT('Ctrl Pts',(14.6988036079793,-0.273200108532066,15.8176504259456));
#5826=CARTESIAN_POINT('Ctrl Pts',(14.6789741278953,-0.241442615310855,15.8439766371743));
#5827=CARTESIAN_POINT('Ctrl Pts',(14.649052119539,-0.174242241359358,15.8790044118403));
#5828=CARTESIAN_POINT('Ctrl Pts',(14.6382480050478,-0.142377760727725,15.8899019417197));
#5829=CARTESIAN_POINT('Ctrl Pts',(14.6253569192039,-0.0844582380039889,
15.9024084088928));
#5830=CARTESIAN_POINT('Ctrl Pts',(14.62170907487,-0.0595388860092602,15.9057258119584));
#5831=CARTESIAN_POINT('Ctrl Pts',(14.6184132964927,-0.0116648059065203,
15.9087259343201));
#5832=CARTESIAN_POINT('Ctrl Pts',(14.6184025825216,0.0111982465765552,15.9087354208236));
#5833=CARTESIAN_POINT('Ctrl Pts',(14.6216515805607,0.0590421319272091,15.9057784384354));
#5834=CARTESIAN_POINT('Ctrl Pts',(14.6252687876419,0.08393313812265,15.9024901407371));
#5835=CARTESIAN_POINT('Ctrl Pts',(14.6380668952534,0.141740583709937,15.8900828025045));
#5836=CARTESIAN_POINT('Ctrl Pts',(14.6487962756114,0.173538618517613,15.8792727935245));
#5837=CARTESIAN_POINT('Ctrl Pts',(14.6782561696043,0.239992102668341,15.8448561504018));
#5838=CARTESIAN_POINT('Ctrl Pts',(14.6976208691953,0.271333339752337,15.8192728778931));
#5839=CARTESIAN_POINT('Ctrl Pts',(14.7371948204043,0.324961457403922,15.7516236294289));
#5840=CARTESIAN_POINT('Ctrl Pts',(14.7561115708548,0.34471876336765,15.709950843486));
#5841=CARTESIAN_POINT('Ctrl Pts',(14.785345858337,0.373200978981364,15.6122094926721));
#5842=CARTESIAN_POINT('Ctrl Pts',(14.793862313091,0.380025791233419,15.556233591069));
#5843=CARTESIAN_POINT('Ctrl Pts',(14.793862313091,0.380025791233419,15.5));
#5844=CARTESIAN_POINT('',(14.793862313091,-0.380025791233415,12.));
#5845=CARTESIAN_POINT('',(14.793862313091,-0.380025791233415,16.));
#5846=CARTESIAN_POINT('Origin',(15.1187936873802,2.22044604925031E-15,12.));
#5847=CARTESIAN_POINT('Origin',(14.6817301172876,-1.34514335437282,16.));
#5848=CARTESIAN_POINT('',(14.6422286690599,-0.846706161149925,15.5));
#5849=CARTESIAN_POINT('',(14.6422286690599,-0.846706161149925,12.));
#5850=CARTESIAN_POINT('',(14.6422286690599,-0.846706161149924,16.));
#5851=CARTESIAN_POINT('',(14.1954815579043,-1.46160080796717,15.5));
#5852=CARTESIAN_POINT('Ctrl Pts',(14.1954815579043,-1.46160080796717,15.5));
#5853=CARTESIAN_POINT('Ctrl Pts',(14.1954815579043,-1.46160080796717,15.5328840768056));
#5854=CARTESIAN_POINT('Ctrl Pts',(14.1945723329548,-1.45798289783153,15.5657453762427));
#5855=CARTESIAN_POINT('Ctrl Pts',(14.1914333807704,-1.44344987510003,15.6296563210017));
#5856=CARTESIAN_POINT('Ctrl Pts',(14.1892159688849,-1.43258484649331,15.660598638283));
#5857=CARTESIAN_POINT('Ctrl Pts',(14.1840274776971,-1.39737620413281,15.7313318911412));
#5858=CARTESIAN_POINT('Ctrl Pts',(14.1811711075199,-1.36973962655568,15.7684373555081));
#5859=CARTESIAN_POINT('Ctrl Pts',(14.1824443852023,-1.30287347205919,15.8299542128302));
#5860=CARTESIAN_POINT('Ctrl Pts',(14.1863901333546,-1.26569203217221,15.8534299122416));
#5861=CARTESIAN_POINT('Ctrl Pts',(14.2058864965607,-1.18626211854957,15.8882855843752));
#5862=CARTESIAN_POINT('Ctrl Pts',(14.2211270097652,-1.14566369972857,15.89904798654));
#5863=CARTESIAN_POINT('Ctrl Pts',(14.2645069510282,-1.06563583469299,15.9101249054252));
#5864=CARTESIAN_POINT('Ctrl Pts',(14.2931370956907,-1.0270489529166,15.9097261007587));
#5865=CARTESIAN_POINT('Ctrl Pts',(14.3582731868495,-0.961108397269499,15.8966960156851));
#5866=CARTESIAN_POINT('Ctrl Pts',(14.3940585533475,-0.93404437578549,15.8843371675477));
#5867=CARTESIAN_POINT('Ctrl Pts',(14.4652898660485,-0.892602752298236,15.8455544418483));
#5868=CARTESIAN_POINT('Ctrl Pts',(14.4990917489119,-0.878620678129173,15.8203829360199));
#5869=CARTESIAN_POINT('Ctrl Pts',(14.5629304927018,-0.858172746774003,15.7531735756887));
#5870=CARTESIAN_POINT('Ctrl Pts',(14.5902458951409,-0.853197206224569,15.7112772176026));
#5871=CARTESIAN_POINT('Ctrl Pts',(14.6311862321619,-0.847224046484188,15.6129247586851));
#5872=CARTESIAN_POINT('Ctrl Pts',(14.6422286690599,-0.846706161149924,15.5565950982509));
#5873=CARTESIAN_POINT('Ctrl Pts',(14.6422286690599,-0.846706161149924,15.5));
#5874=CARTESIAN_POINT('',(14.1954815579043,-1.46160080796717,12.));
#5875=CARTESIAN_POINT('',(14.1954815579043,-1.46160080796717,16.));
#5876=CARTESIAN_POINT('Origin',(14.6817301172876,-1.34514335437282,12.));
#5877=CARTESIAN_POINT('Origin',(13.537482835541,-2.17648766711626,16.));
#5878=CARTESIAN_POINT('',(13.7984995239928,-1.75002513845795,15.5));
#5879=CARTESIAN_POINT('',(13.7984995239928,-1.75002513845795,12.));
#5880=CARTESIAN_POINT('',(13.7984995239928,-1.75002513845795,16.));
#5881=CARTESIAN_POINT('',(13.0756475137673,-1.98489399404177,15.5));
#5882=CARTESIAN_POINT('Ctrl Pts',(13.0756475137673,-1.98489399404178,15.5));
#5883=CARTESIAN_POINT('Ctrl Pts',(13.0756475137673,-1.98489399404178,15.5315974346976));
#5884=CARTESIAN_POINT('Ctrl Pts',(13.076934471735,-1.98169929993151,15.5631757175052));
#5885=CARTESIAN_POINT('Ctrl Pts',(13.0824602699234,-1.96911950577423,15.6247606509986));
#5886=CARTESIAN_POINT('Ctrl Pts',(13.0866862266967,-1.9597668107847,15.6546762688613));
#5887=CARTESIAN_POINT('Ctrl Pts',(13.1021176714653,-1.92978725799424,15.7249493973573));
#5888=CARTESIAN_POINT('Ctrl Pts',(13.1154668528302,-1.906259901776,15.762620760625));
#5889=CARTESIAN_POINT('Ctrl Pts',(13.1545394298129,-1.85338430197355,15.8255830998499));
#5890=CARTESIAN_POINT('Ctrl Pts',(13.1790099156272,-1.82554632233921,15.8498680529139));
#5891=CARTESIAN_POINT('Ctrl Pts',(13.2413375892144,-1.77146870244053,15.8866893895236));
#5892=CARTESIAN_POINT('Ctrl Pts',(13.2782013645668,-1.74656759203558,15.8982106592639));
#5893=CARTESIAN_POINT('Ctrl Pts',(13.3627218526327,-1.70550952857365,15.9102329913456));
#5894=CARTESIAN_POINT('Ctrl Pts',(13.410303944242,-1.69050766300347,15.909874133055));
#5895=CARTESIAN_POINT('Ctrl Pts',(13.5026030116303,-1.67568037378513,15.8963684971709));
#5896=CARTESIAN_POINT('Ctrl Pts',(13.5465650082624,-1.67487990467903,15.8841705706778));
#5897=CARTESIAN_POINT('Ctrl Pts',(13.6280162499368,-1.68306934122621,15.8458060158298));
#5898=CARTESIAN_POINT('Ctrl Pts',(13.6637799617895,-1.69165869793162,15.8205491017219));
#5899=CARTESIAN_POINT('Ctrl Pts',(13.7275857166867,-1.71268387513612,15.7531986669259));
#5900=CARTESIAN_POINT('Ctrl Pts',(13.7526058151867,-1.7247105935723,15.7113185385228));
#5901=CARTESIAN_POINT('Ctrl Pts',(13.7892546800524,-1.74394867728652,15.6129675013504));
#5902=CARTESIAN_POINT('Ctrl Pts',(13.7984995239928,-1.75002513845795,15.5566167040035));
#5903=CARTESIAN_POINT('Ctrl Pts',(13.7984995239928,-1.75002513845795,15.5));
#5904=CARTESIAN_POINT('',(13.0756475137673,-1.98489399404177,12.));
#5905=CARTESIAN_POINT('',(13.0756475137673,-1.98489399404177,16.));
#5906=CARTESIAN_POINT('Origin',(13.537482835541,-2.17648766711626,12.));
#5907=CARTESIAN_POINT('Origin',(12.1231154122328,-2.17648766711627,16.));
#5908=CARTESIAN_POINT('',(12.5849507340066,-1.98489399404177,15.5));
#5909=CARTESIAN_POINT('',(12.5849507340066,-1.98489399404177,12.));
#5910=CARTESIAN_POINT('',(12.5849507340066,-1.98489399404177,16.));
#5911=CARTESIAN_POINT('',(11.862098723781,-1.75002513845795,15.5));
#5912=CARTESIAN_POINT('Ctrl Pts',(11.862098723781,-1.75002513845795,15.5));
#5913=CARTESIAN_POINT('Ctrl Pts',(11.862098723781,-1.75002513845795,15.5315974346976));
#5914=CARTESIAN_POINT('Ctrl Pts',(11.8650176887316,-1.74819703154467,15.5631757175052));
#5915=CARTESIAN_POINT('Ctrl Pts',(11.876882370856,-1.74126774696798,15.6247606509986));
#5916=CARTESIAN_POINT('Ctrl Pts',(11.8857986178871,-1.73618521284643,15.6546762688613));
#5917=CARTESIAN_POINT('Ctrl Pts',(11.9159044579532,-1.72100162081169,15.7249493973573));
#5918=CARTESIAN_POINT('Ctrl Pts',(11.9405332055489,-1.7098140417349,15.762620760625));
#5919=CARTESIAN_POINT('Ctrl Pts',(12.003223082112,-1.69000306742646,15.8255830998499));
#5920=CARTESIAN_POINT('Ctrl Pts',(12.039382874879,-1.68186505949125,15.8498680529139));
#5921=CARTESIAN_POINT('Ctrl Pts',(12.1215930494864,-1.67475063332217,15.8866893895236));
#5922=CARTESIAN_POINT('Ctrl Pts',(12.1660529756851,-1.67627319532172,15.8982106592639));
#5923=CARTESIAN_POINT('Ctrl Pts',(12.2585648110939,-1.69273642062657,15.9102329913456));
#5924=CARTESIAN_POINT('Ctrl Pts',(12.3058774071727,-1.70856770815414,15.909874133055));
#5925=CARTESIAN_POINT('Ctrl Pts',(12.3892641831888,-1.75082420980719,15.8963684971709));
#5926=CARTESIAN_POINT('Ctrl Pts',(12.4253006895064,-1.77601682997858,15.8841705706778));
#5927=CARTESIAN_POINT('Ctrl Pts',(12.4863824982069,-1.83051806195672,15.8458060158298));
#5928=CARTESIAN_POINT('Ctrl Pts',(12.5102672516795,-1.85848837989641,15.8205491017219));
#5929=CARTESIAN_POINT('Ctrl Pts',(12.5495289026426,-1.9130021873045,15.7531986669259));
#5930=CARTESIAN_POINT('Ctrl Pts',(12.5627014597997,-1.93743845181514,15.7113185385228));
#5931=CARTESIAN_POINT('Ctrl Pts',(12.5810431524111,-1.97454405076052,15.6129675013504));
#5932=CARTESIAN_POINT('Ctrl Pts',(12.5849507340066,-1.98489399404177,15.5566167040035));
#5933=CARTESIAN_POINT('Ctrl Pts',(12.5849507340066,-1.98489399404177,15.5));
#5934=CARTESIAN_POINT('',(11.862098723781,-1.75002513845795,12.));
#5935=CARTESIAN_POINT('',(11.862098723781,-1.75002513845795,16.));
#5936=CARTESIAN_POINT('Origin',(12.1231154122328,-2.17648766711627,12.));
#5937=CARTESIAN_POINT('Origin',(10.9788681304862,-1.34514335437282,16.));
#5938=CARTESIAN_POINT('',(11.4651166898695,-1.46160080796717,15.5));
#5939=CARTESIAN_POINT('',(11.4651166898695,-1.46160080796717,12.));
#5940=CARTESIAN_POINT('',(11.4651166898695,-1.46160080796717,16.));
#5941=CARTESIAN_POINT('',(11.0183695787139,-0.846706161149927,15.5));
#5942=CARTESIAN_POINT('Ctrl Pts',(11.0183695787139,-0.846706161149927,15.5));
#5943=CARTESIAN_POINT('Ctrl Pts',(11.0183695787139,-0.846706161149927,15.5327258400527));
#5944=CARTESIAN_POINT('Ctrl Pts',(11.0220556185493,-0.84695739201299,15.5654293765226));
#5945=CARTESIAN_POINT('Ctrl Pts',(11.0367039251324,-0.848445254539305,15.6290406866894));
#5946=CARTESIAN_POINT('Ctrl Pts',(11.0476136300772,-0.849677906933497,15.6598442001574));
#5947=CARTESIAN_POINT('Ctrl Pts',(11.0824957651747,-0.855557203465595,15.7305775282065));
#5948=CARTESIAN_POINT('Ctrl Pts',(11.1096279981436,-0.861340474076375,15.7678051908843));
#5949=CARTESIAN_POINT('Ctrl Pts',(11.1728071364189,-0.883127772807806,15.8295297239576));
#5950=CARTESIAN_POINT('Ctrl Pts',(11.2069557061982,-0.898320369211427,15.853094168515));
#5951=CARTESIAN_POINT('Ctrl Pts',(11.2765325572588,-0.941328440996174,15.8881049113845));
#5952=CARTESIAN_POINT('Ctrl Pts',(11.3104794862702,-0.968336272581112,15.8989286877205));
#5953=CARTESIAN_POINT('Ctrl Pts',(11.3732766333986,-1.0342712261584,15.9101071881998));
#5954=CARTESIAN_POINT('Ctrl Pts',(11.4011761407951,-1.07339769304206,15.909753701168));
#5955=CARTESIAN_POINT('Ctrl Pts',(11.4439702977233,-1.15590790002146,15.8967861544805));
#5956=CARTESIAN_POINT('Ctrl Pts',(11.4587435473851,-1.19853273696263,15.8843843767206));
#5957=CARTESIAN_POINT('Ctrl Pts',(11.4761516255951,-1.27923724113745,15.8454873880819));
#5958=CARTESIAN_POINT('Ctrl Pts',(11.4789959829928,-1.3156527365084,15.8203384131985));
#5959=CARTESIAN_POINT('Ctrl Pts',(11.4787154953012,-1.3826466364114,15.7531662441803));
#5960=CARTESIAN_POINT('Ctrl Pts',(11.4750059464849,-1.41016355466825,15.7112656542922));
#5961=CARTESIAN_POINT('Ctrl Pts',(11.4680357739965,-1.4509410002687,15.6129130718351));
#5962=CARTESIAN_POINT('Ctrl Pts',(11.4651166898695,-1.46160080796717,15.5565891907874));
#5963=CARTESIAN_POINT('Ctrl Pts',(11.4651166898695,-1.46160080796717,15.5));
#5964=CARTESIAN_POINT('',(11.0183695787139,-0.846706161149927,12.));
#5965=CARTESIAN_POINT('',(11.0183695787139,-0.846706161149927,16.));
#5966=CARTESIAN_POINT('Origin',(10.9788681304862,-1.34514335437282,12.));
#5967=CARTESIAN_POINT('Origin',(12.8302991238869,0.,12.));
#5968=CARTESIAN_POINT('Origin',(12.8302991238869,0.,12.));
#5969=CARTESIAN_POINT('Origin',(12.8302991238869,0.,12.));
#5970=CARTESIAN_POINT('Origin',(12.8302991238869,0.,12.));
#5971=CARTESIAN_POINT('Origin',(12.8302991238869,0.,12.));
#5972=CARTESIAN_POINT('Origin',(12.8302991238869,0.,12.));
#5973=CARTESIAN_POINT('Origin',(12.8302991238869,0.,12.));
#5974=CARTESIAN_POINT('Origin',(12.8302991238869,0.,12.));
#5975=CARTESIAN_POINT('Origin',(12.8302991238869,0.,12.));
#5976=CARTESIAN_POINT('',(10.8667359346828,-0.380025791233421,12.));
#5977=CARTESIAN_POINT('Origin',(12.8302991238869,0.,12.));
#5978=CARTESIAN_POINT('',(10.8667359346828,0.380025791233421,12.));
#5979=CARTESIAN_POINT('Origin',(10.5418045603937,0.,12.));
#5980=CARTESIAN_POINT('Origin',(12.8302991238869,0.,12.));
#5981=CARTESIAN_POINT('',(11.8302991238869,-1.22464679914735E-16,12.));
#5982=CARTESIAN_POINT('Origin',(12.8302991238869,0.,12.));
#5983=CARTESIAN_POINT('Origin',(12.8302991238869,0.,12.));
#5984=CARTESIAN_POINT('',(10.8667359346828,-0.38002579123342,15.5));
#5985=CARTESIAN_POINT('Origin',(12.8302991238869,0.,15.5));
#5986=CARTESIAN_POINT('',(10.8667359346828,-0.380025791233421,16.));
#5987=CARTESIAN_POINT('Origin',(12.8302991238869,0.,12.));
#5988=CARTESIAN_POINT('Origin',(12.8302991238869,0.,15.5));
#5989=CARTESIAN_POINT('Origin',(12.8302991238869,0.,12.));
#5990=CARTESIAN_POINT('Origin',(12.8302991238869,0.,15.5));
#5991=CARTESIAN_POINT('Origin',(12.8302991238869,0.,12.));
#5992=CARTESIAN_POINT('Origin',(12.8302991238869,0.,15.5));
#5993=CARTESIAN_POINT('Origin',(12.8302991238869,0.,12.));
#5994=CARTESIAN_POINT('Origin',(12.8302991238869,0.,15.5));
#5995=CARTESIAN_POINT('Origin',(12.8302991238869,0.,12.));
#5996=CARTESIAN_POINT('Origin',(12.8302991238869,0.,15.5));
#5997=CARTESIAN_POINT('Origin',(12.8302991238869,0.,12.));
#5998=CARTESIAN_POINT('Origin',(12.8302991238869,0.,15.5));
#5999=CARTESIAN_POINT('Origin',(12.8302991238869,0.,12.));
#6000=CARTESIAN_POINT('Origin',(12.8302991238869,0.,15.5));
#6001=CARTESIAN_POINT('Origin',(12.8302991238869,0.,12.));
#6002=CARTESIAN_POINT('Origin',(12.8302991238869,0.,15.5));
#6003=CARTESIAN_POINT('Origin',(12.8302991238869,0.,15.5));
#6004=CARTESIAN_POINT('',(11.3302991238869,1.83697019872103E-16,16.));
#6005=CARTESIAN_POINT('Origin',(12.8302991238869,0.,16.));
#6006=CARTESIAN_POINT('',(11.0418045603937,-2.18386077671221E-16,15.9083759136321));
#6007=CARTESIAN_POINT('Origin',(11.3302991238869,-1.83697019872103E-16,
15.5));
#6008=CARTESIAN_POINT('Ctrl Pts',(11.0418045603937,-2.17744741094999E-16,
15.9083759136321));
#6009=CARTESIAN_POINT('Ctrl Pts',(11.0418045603937,-0.0333269392899449,
15.9083759136321));
#6010=CARTESIAN_POINT('Ctrl Pts',(11.0384294338572,-0.0666007585217244,
15.9054111603401));
#6011=CARTESIAN_POINT('Ctrl Pts',(11.0247216398412,-0.134678328230504,15.8922768955596));
#6012=CARTESIAN_POINT('Ctrl Pts',(11.0136953982254,-0.168722451358547,15.8813576283571));
#6013=CARTESIAN_POINT('Ctrl Pts',(10.9836162130091,-0.237730651178781,15.84648748042));
#6014=CARTESIAN_POINT('Ctrl Pts',(10.9641176217848,-0.269612450661452,15.8209662339571));
#6015=CARTESIAN_POINT('Ctrl Pts',(10.9242382544975,-0.324013302894191,15.7533173172479));
#6016=CARTESIAN_POINT('Ctrl Pts',(10.9051561320036,-0.344027884939244,15.7116694990272));
#6017=CARTESIAN_POINT('Ctrl Pts',(10.8754426059288,-0.373057962817857,15.6134141633368));
#6018=CARTESIAN_POINT('Ctrl Pts',(10.8667359346828,-0.380025791233421,15.5568425534222));
#6019=CARTESIAN_POINT('Ctrl Pts',(10.8667359346828,-0.380025791233421,15.5));
#6020=CARTESIAN_POINT('',(10.8667359346828,0.38002579123342,15.5));
#6021=CARTESIAN_POINT('Origin',(12.8302991238869,0.,15.5));
#6022=CARTESIAN_POINT('Ctrl Pts',(10.8667359346828,0.38002579123342,15.5));
#6023=CARTESIAN_POINT('Ctrl Pts',(10.8667359346828,0.38002579123342,15.5287883283061));
#6024=CARTESIAN_POINT('Ctrl Pts',(10.8689246936405,0.378186511904044,15.5575638011946));
#6025=CARTESIAN_POINT('Ctrl Pts',(10.8775010031577,0.370595290430779,15.6141318495287));
#6026=CARTESIAN_POINT('Ctrl Pts',(10.8839020018485,0.364829650654932,15.641855828518));
#6027=CARTESIAN_POINT('Ctrl Pts',(10.9048993108626,0.344216382575075,15.7100185500455));
#6028=CARTESIAN_POINT('Ctrl Pts',(10.9219087613342,0.326315405731202,15.7480224050071));
#6029=CARTESIAN_POINT('Ctrl Pts',(10.9597410970604,0.276288530513651,15.8146310640371));
#6030=CARTESIAN_POINT('Ctrl Pts',(10.9796822362452,0.244921275640039,15.8414816023624));
#6031=CARTESIAN_POINT('Ctrl Pts',(11.0109275363277,0.176276582694249,15.8784425964261));
#6032=CARTESIAN_POINT('Ctrl Pts',(11.0225649861349,0.14226151080342,15.8901343381799));
#6033=CARTESIAN_POINT('Ctrl Pts',(11.0376188560823,0.0729388013115952,15.9046912409227));
#6034=CARTESIAN_POINT('Ctrl Pts',(11.0415308605551,0.0384029564419577,15.9081284852292));
#6035=CARTESIAN_POINT('Ctrl Pts',(11.0417998828598,0.00249739362048287,
15.9083716855965));
#6036=CARTESIAN_POINT('Ctrl Pts',(11.0418045603937,0.0012486595197422,15.9083759136321));
#6037=CARTESIAN_POINT('Ctrl Pts',(11.0418045603937,-2.17744741094999E-16,
15.9083759136321));
#6038=CARTESIAN_POINT('Origin',(10.5418045603937,0.,16.));
#6039=CARTESIAN_POINT('',(10.8667359346828,0.380025791233421,16.));
#6040=CARTESIAN_POINT('Origin',(12.8302991238869,0.,12.));
#6041=CARTESIAN_POINT('Origin',(12.8302991238869,0.,16.));
#6042=CARTESIAN_POINT('Origin',(12.8302991238869,0.,12.));
#6043=CARTESIAN_POINT('',(11.8302991238869,-1.22464679914735E-16,10.));
#6044=CARTESIAN_POINT('Origin',(12.8302991238869,0.,10.));
#6045=CARTESIAN_POINT('',(11.8302991238869,1.22464679914735E-16,12.));
#6046=CARTESIAN_POINT('Origin',(12.8302991238869,0.,10.));
#7295=UNCERTAINTY_MEASURE_WITH_UNIT(LENGTH_MEASURE(0.01),#7316,
'DISTANCE_ACCURACY_VALUE',
'Maximum model space distance between geometric entities at asserted c
onnectivities');
#7303=UNCERTAINTY_MEASURE_WITH_UNIT(LENGTH_MEASURE(0.01),#7316,
'DISTANCE_ACCURACY_VALUE',
'Maximum model space distance between geometric entities at asserted c
onnectivities');
#7307=(
GEOMETRIC_REPRESENTATION_CONTEXT(3)
GLOBAL_UNCERTAINTY_ASSIGNED_CONTEXT((#7295))
GLOBAL_UNIT_ASSIGNED_CONTEXT((#7316,#7318,#7319))
REPRESENTATION_CONTEXT('','3D')
);
#7315=(
GEOMETRIC_REPRESENTATION_CONTEXT(3)
GLOBAL_UNCERTAINTY_ASSIGNED_CONTEXT((#7303))
GLOBAL_UNIT_ASSIGNED_CONTEXT((#7316,#7318,#7319))
REPRESENTATION_CONTEXT('','3D')
);
#7316=(
LENGTH_UNIT()
NAMED_UNIT(*)
SI_UNIT(.MILLI.,.METRE.)
);
#7318=(
NAMED_UNIT(*)
PLANE_ANGLE_UNIT()
SI_UNIT($,.RADIAN.)
);
#7319=(
NAMED_UNIT(*)
SI_UNIT($,.STERADIAN.)
SOLID_ANGLE_UNIT()
);
#7323=SHAPE_DEFINITION_REPRESENTATION(#7334,#7355);
#7334=PRODUCT_DEFINITION_SHAPE('',$,#7367);
#7355=SHAPE_REPRESENTATION('',(#3467),#7307);
#7363=PRODUCT_DEFINITION_CONTEXT('part definition',#7398,'design');
#7367=PRODUCT_DEFINITION('Knob','Knob',#7378,#7363);
#7378=PRODUCT_DEFINITION_FORMATION('',$,#7403);
#7398=APPLICATION_CONTEXT(
'Core Data for Automotive Mechanical Design Process');
#7399=PRODUCT_CONTEXT('part definition',#7398,'mechanical');
#7403=PRODUCT('Knob','Knob',$,(#7399));
#7432=COLOUR_RGB('Sky Blue',0.24,0.69,0.87);
#7433=FILL_AREA_STYLE_COLOUR('',#7432);
#7434=FILL_AREA_STYLE('',(#7433));
#7435=SURFACE_STYLE_FILL_AREA(#7434);
#7436=SURFACE_SIDE_STYLE('',(#7435));
#7437=SURFACE_STYLE_USAGE(.BOTH.,#7436);
#7438=PRESENTATION_STYLE_ASSIGNMENT((#7437));
ENDSEC;
END-ISO-10303-21;
